ISO-10303-21;
HEADER;
/* Generated by software containing ST-Developer
 * from STEP Tools, Inc. (www.steptools.com) 
 */

FILE_DESCRIPTION(
/* description */ ('Gear mesh backlash fixture'),
/* implementation_level */ '2;1');

FILE_NAME(
/* name */ 'Cap Screw - M4x16.step',
/* time_stamp */ '2026-10-28T03:26:00-07:00',
/* author */ (''),
/* organization */ (''),
/* preprocessor_version */ 'ST-DEVELOPER v20.2',
/* originating_system */ 'Autodesk Translation Framework v15.17.0.0',
/* authorisation */ '');

FILE_SCHEMA (('AUTOMOTIVE_DESIGN { 1 0 10303 214 3 1 1 }'));
ENDSEC;

DATA;
#10=MECHANICAL_DESIGN_GEOMETRIC_PRESENTATION_REPRESENTATION('',(#1040),#57900);
#371=ORIENTED_CLOSED_SHELL('',*,#13601,.F.);
#374=BREP_WITH_VOIDS('Body1',#13600,(#371));
#763=CONICAL_SURFACE('',#14627,0.325,0.785398163397448);
#764=CONICAL_SURFACE('',#14631,0.335,0.785398163397448);
#765=CONICAL_SURFACE('',#14635,0.21,0.463647609000806);
#766=CONICAL_SURFACE('',#14639,0.18,0.785398163397448);
#933=SHAPE_REPRESENTATION_RELATIONSHIP('SRR','None',#58129,#983);
#983=ADVANCED_BREP_SHAPE_REPRESENTATION('',(#374),#57862);
#1040=STYLED_ITEM('',(#58472),#374);
#1226=FACE_BOUND('',#2741,.T.);
#1429=PLANE('',#14625);
#1430=PLANE('',#14633);
#1431=PLANE('',#14641);
#1432=PLANE('',#14642);
#1433=PLANE('',#14643);
#1434=PLANE('',#14644);
#1435=PLANE('',#14645);
#1436=PLANE('',#14646);
#1437=PLANE('',#14647);
#1438=PLANE('',#14648);
#1439=PLANE('',#14649);
#1888=FACE_OUTER_BOUND('',#2736,.T.);
#1889=FACE_OUTER_BOUND('',#2737,.T.);
#1890=FACE_OUTER_BOUND('',#2738,.T.);
#1891=FACE_OUTER_BOUND('',#2739,.T.);
#1892=FACE_OUTER_BOUND('',#2740,.T.);
#1893=FACE_OUTER_BOUND('',#2742,.T.);
#1894=FACE_OUTER_BOUND('',#2743,.T.);
#1895=FACE_OUTER_BOUND('',#2744,.T.);
#1896=FACE_OUTER_BOUND('',#2745,.T.);
#1897=FACE_OUTER_BOUND('',#2746,.T.);
#1898=FACE_OUTER_BOUND('',#2747,.T.);
#1899=FACE_OUTER_BOUND('',#2748,.T.);
#1900=FACE_OUTER_BOUND('',#2749,.T.);
#1901=FACE_OUTER_BOUND('',#2750,.T.);
#1902=FACE_OUTER_BOUND('',#2751,.T.);
#1903=FACE_OUTER_BOUND('',#2752,.T.);
#1904=FACE_OUTER_BOUND('',#2753,.T.);
#2736=EDGE_LOOP('',(#9745));
#2737=EDGE_LOOP('',(#9746,#9747,#9748,#9749));
#2738=EDGE_LOOP('',(#9750,#9751,#9752,#9753));
#2739=EDGE_LOOP('',(#9754,#9755,#9756,#9757));
#2740=EDGE_LOOP('',(#9758));
#2741=EDGE_LOOP('',(#9759));
#2742=EDGE_LOOP('',(#9760,#9761,#9762,#9763));
#2743=EDGE_LOOP('',(#9764,#9765,#9766,#9767));
#2744=EDGE_LOOP('',(#9768,#9769,#9770,#9771));
#2745=EDGE_LOOP('',(#9772));
#2746=EDGE_LOOP('',(#9773,#9774,#9775,#9776));
#2747=EDGE_LOOP('',(#9777,#9778,#9779,#9780));
#2748=EDGE_LOOP('',(#9781,#9782,#9783,#9784));
#2749=EDGE_LOOP('',(#9785,#9786,#9787,#9788));
#2750=EDGE_LOOP('',(#9789,#9790,#9791,#9792));
#2751=EDGE_LOOP('',(#9793,#9794,#9795,#9796));
#2752=EDGE_LOOP('',(#9797,#9798,#9799,#9800,#9801,#9802));
#2753=EDGE_LOOP('',(#9803,#9804,#9805,#9806,#9807,#9808));
#3613=LINE('',#20573,#4502);
#3614=LINE('',#20577,#4503);
#3615=LINE('',#20581,#4504);
#3616=LINE('',#20588,#4505);
#3617=LINE('',#20592,#4506);
#3618=LINE('',#20596,#4507);
#3619=LINE('',#20601,#4508);
#3620=LINE('',#20603,#4509);
#3621=LINE('',#20605,#4510);
#3622=LINE('',#20606,#4511);
#3623=LINE('',#20609,#4512);
#3624=LINE('',#20611,#4513);
#3625=LINE('',#20612,#4514);
#3626=LINE('',#20615,#4515);
#3627=LINE('',#20617,#4516);
#3628=LINE('',#20618,#4517);
#3629=LINE('',#20621,#4518);
#3630=LINE('',#20623,#4519);
#3631=LINE('',#20624,#4520);
#3632=LINE('',#20627,#4521);
#3633=LINE('',#20629,#4522);
#3634=LINE('',#20630,#4523);
#3635=LINE('',#20632,#4524);
#3636=LINE('',#20633,#4525);
#4502=VECTOR('',#16648,0.325);
#4503=VECTOR('',#16653,0.35);
#4504=VECTOR('',#16658,0.335);
#4505=VECTOR('',#16667,0.21);
#4506=VECTOR('',#16672,0.2);
#4507=VECTOR('',#16677,0.18);
#4508=VECTOR('',#16682,1.);
#4509=VECTOR('',#16683,1.);
#4510=VECTOR('',#16684,1.);
#4511=VECTOR('',#16685,1.);
#4512=VECTOR('',#16688,1.);
#4513=VECTOR('',#16689,1.);
#4514=VECTOR('',#16690,1.);
#4515=VECTOR('',#16693,1.);
#4516=VECTOR('',#16694,1.);
#4517=VECTOR('',#16695,1.);
#4518=VECTOR('',#16698,1.);
#4519=VECTOR('',#16699,1.);
#4520=VECTOR('',#16700,1.);
#4521=VECTOR('',#16703,1.);
#4522=VECTOR('',#16704,1.);
#4523=VECTOR('',#16705,1.);
#4524=VECTOR('',#16708,1.);
#4525=VECTOR('',#16709,1.);
#5399=CIRCLE('',#14626,0.3);
#5400=CIRCLE('',#14628,0.35);
#5401=CIRCLE('',#14630,0.35);
#5402=CIRCLE('',#14632,0.32);
#5403=CIRCLE('',#14634,0.22);
#5404=CIRCLE('',#14636,0.1954);
#5405=CIRCLE('',#14638,0.1954);
#5406=CIRCLE('',#14640,0.16);
#6073=VERTEX_POINT('',#20568);
#6074=VERTEX_POINT('',#20571);
#6075=VERTEX_POINT('',#20575);
#6076=VERTEX_POINT('',#20579);
#6077=VERTEX_POINT('',#20583);
#6078=VERTEX_POINT('',#20586);
#6079=VERTEX_POINT('',#20590);
#6080=VERTEX_POINT('',#20594);
#6081=VERTEX_POINT('',#20599);
#6082=VERTEX_POINT('',#20600);
#6083=VERTEX_POINT('',#20602);
#6084=VERTEX_POINT('',#20604);
#6085=VERTEX_POINT('',#20608);
#6086=VERTEX_POINT('',#20610);
#6087=VERTEX_POINT('',#20614);
#6088=VERTEX_POINT('',#20616);
#6089=VERTEX_POINT('',#20620);
#6090=VERTEX_POINT('',#20622);
#6091=VERTEX_POINT('',#20626);
#6092=VERTEX_POINT('',#20628);
#7459=EDGE_CURVE('',#6073,#6073,#5399,.T.);
#7460=EDGE_CURVE('',#6074,#6074,#5400,.T.);
#7461=EDGE_CURVE('',#6074,#6073,#3613,.T.);
#7462=EDGE_CURVE('',#6075,#6075,#5401,.T.);
#7463=EDGE_CURVE('',#6075,#6074,#3614,.T.);
#7464=EDGE_CURVE('',#6076,#6076,#5402,.T.);
#7465=EDGE_CURVE('',#6076,#6075,#3615,.T.);
#7466=EDGE_CURVE('',#6077,#6077,#5403,.T.);
#7467=EDGE_CURVE('',#6078,#6078,#5404,.F.);
#7468=EDGE_CURVE('',#6078,#6077,#3616,.T.);
#7469=EDGE_CURVE('',#6079,#6079,#5405,.F.);
#7470=EDGE_CURVE('',#6079,#6078,#3617,.T.);
#7471=EDGE_CURVE('',#6080,#6080,#5406,.T.);
#7472=EDGE_CURVE('',#6080,#6079,#3618,.T.);
#7473=EDGE_CURVE('',#6081,#6082,#3619,.T.);
#7474=EDGE_CURVE('',#6082,#6083,#3620,.T.);
#7475=EDGE_CURVE('',#6083,#6084,#3621,.T.);
#7476=EDGE_CURVE('',#6081,#6084,#3622,.T.);
#7477=EDGE_CURVE('',#6082,#6085,#3623,.T.);
#7478=EDGE_CURVE('',#6085,#6086,#3624,.T.);
#7479=EDGE_CURVE('',#6086,#6083,#3625,.T.);
#7480=EDGE_CURVE('',#6085,#6087,#3626,.T.);
#7481=EDGE_CURVE('',#6087,#6088,#3627,.T.);
#7482=EDGE_CURVE('',#6088,#6086,#3628,.T.);
#7483=EDGE_CURVE('',#6087,#6089,#3629,.T.);
#7484=EDGE_CURVE('',#6089,#6090,#3630,.T.);
#7485=EDGE_CURVE('',#6090,#6088,#3631,.T.);
#7486=EDGE_CURVE('',#6089,#6091,#3632,.T.);
#7487=EDGE_CURVE('',#6091,#6092,#3633,.T.);
#7488=EDGE_CURVE('',#6092,#6090,#3634,.T.);
#7489=EDGE_CURVE('',#6091,#6081,#3635,.T.);
#7490=EDGE_CURVE('',#6084,#6092,#3636,.T.);
#9745=ORIENTED_EDGE('',*,*,#7459,.F.);
#9746=ORIENTED_EDGE('',*,*,#7460,.F.);
#9747=ORIENTED_EDGE('',*,*,#7461,.T.);
#9748=ORIENTED_EDGE('',*,*,#7459,.T.);
#9749=ORIENTED_EDGE('',*,*,#7461,.F.);
#9750=ORIENTED_EDGE('',*,*,#7462,.F.);
#9751=ORIENTED_EDGE('',*,*,#7463,.T.);
#9752=ORIENTED_EDGE('',*,*,#7460,.T.);
#9753=ORIENTED_EDGE('',*,*,#7463,.F.);
#9754=ORIENTED_EDGE('',*,*,#7464,.F.);
#9755=ORIENTED_EDGE('',*,*,#7465,.T.);
#9756=ORIENTED_EDGE('',*,*,#7462,.T.);
#9757=ORIENTED_EDGE('',*,*,#7465,.F.);
#9758=ORIENTED_EDGE('',*,*,#7464,.T.);
#9759=ORIENTED_EDGE('',*,*,#7466,.F.);
#9760=ORIENTED_EDGE('',*,*,#7467,.F.);
#9761=ORIENTED_EDGE('',*,*,#7468,.T.);
#9762=ORIENTED_EDGE('',*,*,#7466,.T.);
#9763=ORIENTED_EDGE('',*,*,#7468,.F.);
#9764=ORIENTED_EDGE('',*,*,#7469,.F.);
#9765=ORIENTED_EDGE('',*,*,#7470,.T.);
#9766=ORIENTED_EDGE('',*,*,#7467,.T.);
#9767=ORIENTED_EDGE('',*,*,#7470,.F.);
#9768=ORIENTED_EDGE('',*,*,#7471,.F.);
#9769=ORIENTED_EDGE('',*,*,#7472,.T.);
#9770=ORIENTED_EDGE('',*,*,#7469,.T.);
#9771=ORIENTED_EDGE('',*,*,#7472,.F.);
#9772=ORIENTED_EDGE('',*,*,#7471,.T.);
#9773=ORIENTED_EDGE('',*,*,#7473,.T.);
#9774=ORIENTED_EDGE('',*,*,#7474,.T.);
#9775=ORIENTED_EDGE('',*,*,#7475,.T.);
#9776=ORIENTED_EDGE('',*,*,#7476,.F.);
#9777=ORIENTED_EDGE('',*,*,#7477,.T.);
#9778=ORIENTED_EDGE('',*,*,#7478,.T.);
#9779=ORIENTED_EDGE('',*,*,#7479,.T.);
#9780=ORIENTED_EDGE('',*,*,#7474,.F.);
#9781=ORIENTED_EDGE('',*,*,#7480,.T.);
#9782=ORIENTED_EDGE('',*,*,#7481,.T.);
#9783=ORIENTED_EDGE('',*,*,#7482,.T.);
#9784=ORIENTED_EDGE('',*,*,#7478,.F.);
#9785=ORIENTED_EDGE('',*,*,#7483,.T.);
#9786=ORIENTED_EDGE('',*,*,#7484,.T.);
#9787=ORIENTED_EDGE('',*,*,#7485,.T.);
#9788=ORIENTED_EDGE('',*,*,#7481,.F.);
#9789=ORIENTED_EDGE('',*,*,#7486,.T.);
#9790=ORIENTED_EDGE('',*,*,#7487,.T.);
#9791=ORIENTED_EDGE('',*,*,#7488,.T.);
#9792=ORIENTED_EDGE('',*,*,#7484,.F.);
#9793=ORIENTED_EDGE('',*,*,#7489,.T.);
#9794=ORIENTED_EDGE('',*,*,#7476,.T.);
#9795=ORIENTED_EDGE('',*,*,#7490,.T.);
#9796=ORIENTED_EDGE('',*,*,#7487,.F.);
#9797=ORIENTED_EDGE('',*,*,#7489,.F.);
#9798=ORIENTED_EDGE('',*,*,#7486,.F.);
#9799=ORIENTED_EDGE('',*,*,#7483,.F.);
#9800=ORIENTED_EDGE('',*,*,#7480,.F.);
#9801=ORIENTED_EDGE('',*,*,#7477,.F.);
#9802=ORIENTED_EDGE('',*,*,#7473,.F.);
#9803=ORIENTED_EDGE('',*,*,#7490,.F.);
#9804=ORIENTED_EDGE('',*,*,#7475,.F.);
#9805=ORIENTED_EDGE('',*,*,#7479,.F.);
#9806=ORIENTED_EDGE('',*,*,#7482,.F.);
#9807=ORIENTED_EDGE('',*,*,#7485,.F.);
#9808=ORIENTED_EDGE('',*,*,#7488,.F.);
#12660=CYLINDRICAL_SURFACE('',#14629,0.35);
#12661=CYLINDRICAL_SURFACE('',#14637,0.1954);
#13005=ADVANCED_FACE('',(#1888),#1429,.T.);
#13006=ADVANCED_FACE('',(#1889),#763,.T.);
#13007=ADVANCED_FACE('',(#1890),#12660,.T.);
#13008=ADVANCED_FACE('',(#1891),#764,.T.);
#13009=ADVANCED_FACE('',(#1892,#1226),#1430,.T.);
#13010=ADVANCED_FACE('',(#1893),#765,.T.);
#13011=ADVANCED_FACE('',(#1894),#12661,.T.);
#13012=ADVANCED_FACE('',(#1895),#766,.T.);
#13013=ADVANCED_FACE('',(#1896),#1431,.T.);
#13014=ADVANCED_FACE('',(#1897),#1432,.F.);
#13015=ADVANCED_FACE('',(#1898),#1433,.F.);
#13016=ADVANCED_FACE('',(#1899),#1434,.F.);
#13017=ADVANCED_FACE('',(#1900),#1435,.F.);
#13018=ADVANCED_FACE('',(#1901),#1436,.F.);
#13019=ADVANCED_FACE('',(#1902),#1437,.F.);
#13020=ADVANCED_FACE('',(#1903),#1438,.F.);
#13021=ADVANCED_FACE('',(#1904),#1439,.F.);
#13600=CLOSED_SHELL('',(#13005,#13006,#13007,#13008,#13009,#13010,#13011,
#13012,#13013));
#13601=CLOSED_SHELL('',(#13014,#13015,#13016,#13017,#13018,#13019,#13020,
#13021));
#14624=AXIS2_PLACEMENT_3D('',#20566,#16638,#16639);
#14625=AXIS2_PLACEMENT_3D('',#20567,#16640,#16641);
#14626=AXIS2_PLACEMENT_3D('',#20569,#16642,#16643);
#14627=AXIS2_PLACEMENT_3D('',#20570,#16644,#16645);
#14628=AXIS2_PLACEMENT_3D('',#20572,#16646,#16647);
#14629=AXIS2_PLACEMENT_3D('',#20574,#16649,#16650);
#14630=AXIS2_PLACEMENT_3D('',#20576,#16651,#16652);
#14631=AXIS2_PLACEMENT_3D('',#20578,#16654,#16655);
#14632=AXIS2_PLACEMENT_3D('',#20580,#16656,#16657);
#14633=AXIS2_PLACEMENT_3D('',#20582,#16659,#16660);
#14634=AXIS2_PLACEMENT_3D('',#20584,#16661,#16662);
#14635=AXIS2_PLACEMENT_3D('',#20585,#16663,#16664);
#14636=AXIS2_PLACEMENT_3D('',#20587,#16665,#16666);
#14637=AXIS2_PLACEMENT_3D('',#20589,#16668,#16669);
#14638=AXIS2_PLACEMENT_3D('',#20591,#16670,#16671);
#14639=AXIS2_PLACEMENT_3D('',#20593,#16673,#16674);
#14640=AXIS2_PLACEMENT_3D('',#20595,#16675,#16676);
#14641=AXIS2_PLACEMENT_3D('',#20597,#16678,#16679);
#14642=AXIS2_PLACEMENT_3D('',#20598,#16680,#16681);
#14643=AXIS2_PLACEMENT_3D('',#20607,#16686,#16687);
#14644=AXIS2_PLACEMENT_3D('',#20613,#16691,#16692);
#14645=AXIS2_PLACEMENT_3D('',#20619,#16696,#16697);
#14646=AXIS2_PLACEMENT_3D('',#20625,#16701,#16702);
#14647=AXIS2_PLACEMENT_3D('',#20631,#16706,#16707);
#14648=AXIS2_PLACEMENT_3D('',#20634,#16710,#16711);
#14649=AXIS2_PLACEMENT_3D('',#20635,#16712,#16713);
#16638=DIRECTION('axis',(0.,0.,1.));
#16639=DIRECTION('refdir',(1.,0.,0.));
#16640=DIRECTION('center_axis',(0.,1.,0.));
#16641=DIRECTION('ref_axis',(0.,0.,1.));
#16642=DIRECTION('center_axis',(0.,-1.,0.));
#16643=DIRECTION('ref_axis',(1.,0.,0.));
#16644=DIRECTION('center_axis',(0.,-1.,0.));
#16645=DIRECTION('ref_axis',(1.,0.,0.));
#16646=DIRECTION('center_axis',(0.,-1.,0.));
#16647=DIRECTION('ref_axis',(1.,0.,0.));
#16648=DIRECTION('',(0.707106781186547,0.707106781186548,8.65956056235493E-17));
#16649=DIRECTION('center_axis',(0.,-1.,0.));
#16650=DIRECTION('ref_axis',(1.,0.,0.));
#16651=DIRECTION('center_axis',(0.,-1.,0.));
#16652=DIRECTION('ref_axis',(1.,0.,0.));
#16653=DIRECTION('',(0.,1.,0.));
#16654=DIRECTION('center_axis',(0.,1.,0.));
#16655=DIRECTION('ref_axis',(1.,0.,0.));
#16656=DIRECTION('center_axis',(0.,-1.,0.));
#16657=DIRECTION('ref_axis',(1.,0.,0.));
#16658=DIRECTION('',(-0.707106781186547,0.707106781186548,-8.65956056235493E-17));
#16659=DIRECTION('center_axis',(0.,-1.,0.));
#16660=DIRECTION('ref_axis',(0.,0.,-1.));
#16661=DIRECTION('center_axis',(0.,-1.,0.));
#16662=DIRECTION('ref_axis',(1.,0.,0.));
#16663=DIRECTION('center_axis',(0.,1.,0.));
#16664=DIRECTION('ref_axis',(1.,0.,0.));
#16665=DIRECTION('center_axis',(0.,1.,0.));
#16666=DIRECTION('ref_axis',(1.,0.,0.));
#16667=DIRECTION('',(-0.447213595499958,0.894427190999916,-5.47678698264203E-17));
#16668=DIRECTION('center_axis',(0.,-1.,0.));
#16669=DIRECTION('ref_axis',(1.,0.,0.));
#16670=DIRECTION('center_axis',(0.,1.,0.));
#16671=DIRECTION('ref_axis',(1.,0.,0.));
#16672=DIRECTION('',(0.,1.,0.));
#16673=DIRECTION('center_axis',(0.,1.,0.));
#16674=DIRECTION('ref_axis',(1.,0.,0.));
#16675=DIRECTION('center_axis',(0.,-1.,0.));
#16676=DIRECTION('ref_axis',(1.,0.,0.));
#16677=DIRECTION('',(-0.707106781186547,0.707106781186548,-8.65956056235493E-17));
#16678=DIRECTION('center_axis',(0.,-1.,0.));
#16679=DIRECTION('ref_axis',(0.,0.,-1.));
#16680=DIRECTION('center_axis',(0.866025403784439,0.,-0.5));
#16681=DIRECTION('ref_axis',(0.5,0.,0.866025403784439));
#16682=DIRECTION('',(-0.5,0.,-0.866025403784439));
#16683=DIRECTION('',(0.,-1.,0.));
#16684=DIRECTION('',(0.5,0.,0.866025403784439));
#16685=DIRECTION('',(0.,-1.,0.));
#16686=DIRECTION('center_axis',(1.60246890531964E-16,0.,-1.));
#16687=DIRECTION('ref_axis',(1.,0.,1.60246890531964E-16));
#16688=DIRECTION('',(-1.,0.,-1.60246890531964E-16));
#16689=DIRECTION('',(0.,-1.,0.));
#16690=DIRECTION('',(1.,0.,1.60246890531964E-16));
#16691=DIRECTION('center_axis',(-0.866025403784439,0.,-0.5));
#16692=DIRECTION('ref_axis',(0.5,0.,-0.866025403784439));
#16693=DIRECTION('',(-0.5,0.,0.866025403784439));
#16694=DIRECTION('',(0.,-1.,0.));
#16695=DIRECTION('',(0.5,0.,-0.866025403784439));
#16696=DIRECTION('center_axis',(-0.866025403784439,0.,0.5));
#16697=DIRECTION('ref_axis',(-0.5,0.,-0.866025403784439));
#16698=DIRECTION('',(0.5,0.,0.866025403784439));
#16699=DIRECTION('',(0.,-1.,0.));
#16700=DIRECTION('',(-0.5,0.,-0.866025403784439));
#16701=DIRECTION('center_axis',(-1.60246890531964E-16,0.,1.));
#16702=DIRECTION('ref_axis',(-1.,0.,-1.60246890531964E-16));
#16703=DIRECTION('',(1.,0.,1.60246890531964E-16));
#16704=DIRECTION('',(0.,-1.,0.));
#16705=DIRECTION('',(-1.,0.,-1.60246890531964E-16));
#16706=DIRECTION('center_axis',(0.866025403784439,0.,0.5));
#16707=DIRECTION('ref_axis',(-0.5,0.,0.866025403784439));
#16708=DIRECTION('',(0.5,0.,-0.866025403784439));
#16709=DIRECTION('',(-0.5,0.,0.866025403784439));
#16710=DIRECTION('center_axis',(0.,1.,0.));
#16711=DIRECTION('ref_axis',(1.,0.,0.));
#16712=DIRECTION('center_axis',(0.,-1.,0.));
#16713=DIRECTION('ref_axis',(0.,0.,-1.));
#20566=CARTESIAN_POINT('',(0.,0.,0.));
#20567=CARTESIAN_POINT('Origin',(0.3,0.4,0.));
#20568=CARTESIAN_POINT('',(-0.3,0.4,-3.67394039744206E-17));
#20569=CARTESIAN_POINT('Origin',(0.,0.4,0.));
#20570=CARTESIAN_POINT('Origin',(0.,0.375,0.));
#20571=CARTESIAN_POINT('',(-0.35,0.35,-4.28626379701573E-17));
#20572=CARTESIAN_POINT('Origin',(0.,0.35,0.));
#20573=CARTESIAN_POINT('',(-0.325,0.375,-3.9801020972289E-17));
#20574=CARTESIAN_POINT('Origin',(0.,0.19,0.));
#20575=CARTESIAN_POINT('',(-0.35,0.03,-4.28626379701574E-17));
#20576=CARTESIAN_POINT('Origin',(0.,0.03,0.));
#20577=CARTESIAN_POINT('',(-0.35,0.19,-4.28626379701574E-17));
#20578=CARTESIAN_POINT('Origin',(0.,0.0149999999999999,0.));
#20579=CARTESIAN_POINT('',(-0.32,-3.29597460435593E-17,-3.91886975727153E-17));
#20580=CARTESIAN_POINT('Origin',(0.,0.,0.));
#20581=CARTESIAN_POINT('',(-0.335,0.0149999999999999,-4.10256677714363E-17));
#20582=CARTESIAN_POINT('Origin',(0.22,0.,0.));
#20583=CARTESIAN_POINT('',(-0.22,-6.93889390390723E-18,-2.69422295812418E-17));
#20584=CARTESIAN_POINT('Origin',(0.,0.,0.));
#20585=CARTESIAN_POINT('Origin',(0.,-0.02,0.));
#20586=CARTESIAN_POINT('',(-0.1954,-0.0492,2.39295984553393E-17));
#20587=CARTESIAN_POINT('Origin',(0.,-0.0492,0.));
#20588=CARTESIAN_POINT('',(-0.21,-0.02,-2.57175827820944E-17));
#20589=CARTESIAN_POINT('Origin',(0.,-0.8,0.));
#20590=CARTESIAN_POINT('',(-0.1954,-1.5646,2.39295984553393E-17));
#20591=CARTESIAN_POINT('Origin',(0.,-1.5646,0.));
#20592=CARTESIAN_POINT('',(-0.1954,-0.8,-2.39295984553393E-17));
#20593=CARTESIAN_POINT('Origin',(0.,-1.58,0.));
#20594=CARTESIAN_POINT('',(-0.16,-1.6,-1.95943487863577E-17));
#20595=CARTESIAN_POINT('Origin',(0.,-1.6,0.));
#20596=CARTESIAN_POINT('',(-0.18,-1.58,-2.20436423846524E-17));
#20597=CARTESIAN_POINT('Origin',(0.,-1.6,0.));
#20598=CARTESIAN_POINT('Origin',(0.0866025403784439,-0.4,-0.15));
#20599=CARTESIAN_POINT('',(0.173205080756888,-0.4,0.));
#20600=CARTESIAN_POINT('',(0.0866025403784439,-0.4,-0.15));
#20601=CARTESIAN_POINT('',(0.173205080756888,-0.4,0.));
#20602=CARTESIAN_POINT('',(0.0866025403784439,-0.64,-0.15));
#20603=CARTESIAN_POINT('',(0.0866025403784439,-0.4,-0.15));
#20604=CARTESIAN_POINT('',(0.173205080756888,-0.64,0.));
#20605=CARTESIAN_POINT('',(0.173205080756888,-0.64,0.));
#20606=CARTESIAN_POINT('',(0.173205080756888,-0.4,0.));
#20607=CARTESIAN_POINT('Origin',(-0.0866025403784438,-0.4,-0.15));
#20608=CARTESIAN_POINT('',(-0.0866025403784438,-0.4,-0.15));
#20609=CARTESIAN_POINT('',(0.0866025403784439,-0.4,-0.15));
#20610=CARTESIAN_POINT('',(-0.0866025403784438,-0.64,-0.15));
#20611=CARTESIAN_POINT('',(-0.0866025403784438,-0.4,-0.15));
#20612=CARTESIAN_POINT('',(0.0866025403784439,-0.64,-0.15));
#20613=CARTESIAN_POINT('Origin',(-0.173205080756888,-0.4,-2.77555756156289E-17));
#20614=CARTESIAN_POINT('',(-0.173205080756888,-0.4,-2.12115047744981E-17));
#20615=CARTESIAN_POINT('',(-0.0866025403784438,-0.4,-0.15));
#20616=CARTESIAN_POINT('',(-0.173205080756888,-0.64,-2.77555756156289E-17));
#20617=CARTESIAN_POINT('',(-0.173205080756888,-0.4,-2.12115047744981E-17));
#20618=CARTESIAN_POINT('',(-0.0866025403784438,-0.64,-0.15));
#20619=CARTESIAN_POINT('Origin',(-0.0866025403784439,-0.4,0.15));
#20620=CARTESIAN_POINT('',(-0.0866025403784439,-0.4,0.15));
#20621=CARTESIAN_POINT('',(-0.173205080756888,-0.4,-2.12115047744981E-17));
#20622=CARTESIAN_POINT('',(-0.0866025403784439,-0.64,0.15));
#20623=CARTESIAN_POINT('',(-0.0866025403784439,-0.4,0.15));
#20624=CARTESIAN_POINT('',(-0.173205080756888,-0.64,-2.12115047744981E-17));
#20625=CARTESIAN_POINT('Origin',(0.0866025403784439,-0.4,0.15));
#20626=CARTESIAN_POINT('',(0.0866025403784439,-0.4,0.15));
#20627=CARTESIAN_POINT('',(-0.0866025403784439,-0.4,0.15));
#20628=CARTESIAN_POINT('',(0.0866025403784439,-0.64,0.15));
#20629=CARTESIAN_POINT('',(0.0866025403784439,-0.4,0.15));
#20630=CARTESIAN_POINT('',(-0.0866025403784439,-0.64,0.15));
#20631=CARTESIAN_POINT('Origin',(0.173205080756888,-0.4,0.));
#20632=CARTESIAN_POINT('',(0.0866025403784439,-0.4,0.15));
#20633=CARTESIAN_POINT('',(0.0866025403784439,-0.64,0.15));
#20634=CARTESIAN_POINT('Origin',(0.,-0.4,-2.77555756156289E-17));
#20635=CARTESIAN_POINT('Origin',(0.,-0.64,-2.77555756156289E-17));
#57803=UNCERTAINTY_MEASURE_WITH_UNIT(LENGTH_MEASURE(0.001),#57901,
'DISTANCE_ACCURACY_VALUE',
'Maximum model space distance between geometric entities at asserted c
onnectivities');
#57841=UNCERTAINTY_MEASURE_WITH_UNIT(LENGTH_MEASURE(0.001),#57901,
'DISTANCE_ACCURACY_VALUE',
'Maximum model space distance between geometric entities at asserted c
onnectivities');
#57862=(
GEOMETRIC_REPRESENTATION_CONTEXT(3)
GLOBAL_UNCERTAINTY_ASSIGNED_CONTEXT((#57803))
GLOBAL_UNIT_ASSIGNED_CONTEXT((#57901,#57903,#57904))
REPRESENTATION_CONTEXT('','3D')
);
#57900=(
GEOMETRIC_REPRESENTATION_CONTEXT(3)
GLOBAL_UNCERTAINTY_ASSIGNED_CONTEXT((#57841))
GLOBAL_UNIT_ASSIGNED_CONTEXT((#57901,#57903,#57904))
REPRESENTATION_CONTEXT('','3D')
);
#57901=(
LENGTH_UNIT()
NAMED_UNIT(*)
SI_UNIT(.CENTI.,.METRE.)
);
#57903=(
NAMED_UNIT(*)
PLANE_ANGLE_UNIT()
SI_UNIT($,.RADIAN.)
);
#57904=(
NAMED_UNIT(*)
SI_UNIT($,.STERADIAN.)
SOLID_ANGLE_UNIT()
);
#57925=SHAPE_DEFINITION_REPRESENTATION(#57988,#58129);
#57988=PRODUCT_DEFINITION_SHAPE('',$,#58188);
#58129=SHAPE_REPRESENTATION('',(#14624),#57862);
#58167=PRODUCT_DEFINITION_CONTEXT('part definition',#58343,'design');
#58188=PRODUCT_DEFINITION('Cap Screw - M4x16','Cap Screw - M4x16',#58246,
#58167);
#58246=PRODUCT_DEFINITION_FORMATION('',$,#58365);
#58343=APPLICATION_CONTEXT(
'Core Data for Automotive Mechanical Design Process');
#58344=PRODUCT_CONTEXT('part definition',#58343,'mechanical');
#58365=PRODUCT('Cap Screw - M4x16','Cap Screw - M4x16',
'Cap Screw - M4x16',(#58344));
#58466=COLOUR_RGB('Black',0.12,0.14,0.17);
#58467=FILL_AREA_STYLE_COLOUR('',#58466);
#58468=FILL_AREA_STYLE('',(#58467));
#58469=SURFACE_STYLE_FILL_AREA(#58468);
#58470=SURFACE_SIDE_STYLE('',(#58469));
#58471=SURFACE_STYLE_USAGE(.BOTH.,#58470);
#58472=PRESENTATION_STYLE_ASSIGNMENT((#58471));
ENDSEC;
END-ISO-10303-21;
